ISO-10303-21;
HEADER;
/* Generated by software containing ST-Developer
 * from STEP Tools, Inc. (www.steptools.com) 
 */

FILE_DESCRIPTION(
/* description */ ('PAT-091'),
/* implementation_level */ '2;1');

FILE_NAME(
/* name */ 'M4 low-profile retaining screw (5).step',
/* time_stamp */ '2026-10-27T15:34:44-07:00',
/* author */ (''),
/* organization */ (''),
/* preprocessor_version */ 'ST-DEVELOPER v20.2',
/* originating_system */ 'Autodesk Translation Framework v15.17.0.0',
/* authorisation */ '');

FILE_SCHEMA (('AUTOMOTIVE_DESIGN { 1 0 10303 214 3 1 1 }'));
ENDSEC;

DATA;
#10=MECHANICAL_DESIGN_GEOMETRIC_PRESENTATION_REPRESENTATION('',(#1054),#25100);
#834=SHAPE_REPRESENTATION_RELATIONSHIP('SRR','None',#25601,#944);
#944=ADVANCED_BREP_SHAPE_REPRESENTATION('',(#1175),#25071);
#1054=STYLED_ITEM('',(#26198),#1175);
#1175=MANIFOLD_SOLID_BREP('Body1',#13334);
#1568=FACE_BOUND('',#3851,.T.);
#1977=PLANE('',#15923);
#1978=PLANE('',#15928);
#1979=PLANE('',#15931);
#2679=FACE_OUTER_BOUND('',#3850,.T.);
#2680=FACE_OUTER_BOUND('',#3852,.T.);
#2681=FACE_OUTER_BOUND('',#3853,.T.);
#2682=FACE_OUTER_BOUND('',#3854,.T.);
#2683=FACE_OUTER_BOUND('',#3855,.T.);
#3850=EDGE_LOOP('',(#11390));
#3851=EDGE_LOOP('',(#11391));
#3852=EDGE_LOOP('',(#11392,#11393,#11394,#11395));
#3853=EDGE_LOOP('',(#11396));
#3854=EDGE_LOOP('',(#11397,#11398,#11399,#11400));
#3855=EDGE_LOOP('',(#11401));
#4773=LINE('',#23827,#5513);
#4774=LINE('',#23831,#5514);
#5513=VECTOR('',#19803,0.350000000000001);
#5514=VECTOR('',#19808,0.199999999999999);
#6160=CIRCLE('',#15924,0.350000000000001);
#6161=CIRCLE('',#15925,0.199999999999999);
#6162=CIRCLE('',#15927,0.350000000000001);
#6163=CIRCLE('',#15930,0.199999999999999);
#7185=VERTEX_POINT('',#23820);
#7186=VERTEX_POINT('',#23822);
#7187=VERTEX_POINT('',#23825);
#7188=VERTEX_POINT('',#23830);
#8630=EDGE_CURVE('',#7185,#7185,#6160,.T.);
#8631=EDGE_CURVE('',#7186,#7186,#6161,.T.);
#8632=EDGE_CURVE('',#7187,#7187,#6162,.T.);
#8633=EDGE_CURVE('',#7187,#7185,#4773,.T.);
#8634=EDGE_CURVE('',#7186,#7188,#4774,.T.);
#8635=EDGE_CURVE('',#7188,#7188,#6163,.T.);
#11390=ORIENTED_EDGE('',*,*,#8630,.F.);
#11391=ORIENTED_EDGE('',*,*,#8631,.T.);
#11392=ORIENTED_EDGE('',*,*,#8632,.F.);
#11393=ORIENTED_EDGE('',*,*,#8633,.T.);
#11394=ORIENTED_EDGE('',*,*,#8630,.T.);
#11395=ORIENTED_EDGE('',*,*,#8633,.F.);
#11396=ORIENTED_EDGE('',*,*,#8632,.T.);
#11397=ORIENTED_EDGE('',*,*,#8631,.F.);
#11398=ORIENTED_EDGE('',*,*,#8634,.T.);
#11399=ORIENTED_EDGE('',*,*,#8635,.T.);
#11400=ORIENTED_EDGE('',*,*,#8634,.F.);
#11401=ORIENTED_EDGE('',*,*,#8635,.F.);
#12341=CYLINDRICAL_SURFACE('',#15926,0.350000000000001);
#12342=CYLINDRICAL_SURFACE('',#15929,0.199999999999999);
#13046=ADVANCED_FACE('',(#2679,#1568),#1977,.F.);
#13047=ADVANCED_FACE('',(#2680),#12341,.T.);
#13048=ADVANCED_FACE('',(#2681),#1978,.T.);
#13049=ADVANCED_FACE('',(#2682),#12342,.T.);
#13050=ADVANCED_FACE('',(#2683),#1979,.F.);
#13334=CLOSED_SHELL('',(#13046,#13047,#13048,#13049,#13050));
#15922=AXIS2_PLACEMENT_3D('',#23818,#19791,#19792);
#15923=AXIS2_PLACEMENT_3D('',#23819,#19793,#19794);
#15924=AXIS2_PLACEMENT_3D('',#23821,#19795,#19796);
#15925=AXIS2_PLACEMENT_3D('',#23823,#19797,#19798);
#15926=AXIS2_PLACEMENT_3D('',#23824,#19799,#19800);
#15927=AXIS2_PLACEMENT_3D('',#23826,#19801,#19802);
#15928=AXIS2_PLACEMENT_3D('',#23828,#19804,#19805);
#15929=AXIS2_PLACEMENT_3D('',#23829,#19806,#19807);
#15930=AXIS2_PLACEMENT_3D('',#23832,#19809,#19810);
#15931=AXIS2_PLACEMENT_3D('',#23833,#19811,#19812);
#19791=DIRECTION('axis',(0.,0.,1.));
#19792=DIRECTION('refdir',(1.,0.,0.));
#19793=DIRECTION('center_axis',(0.,1.,0.));
#19794=DIRECTION('ref_axis',(1.,0.,0.));
#19795=DIRECTION('center_axis',(0.,1.,0.));
#19796=DIRECTION('ref_axis',(1.,0.,0.));
#19797=DIRECTION('center_axis',(0.,1.,0.));
#19798=DIRECTION('ref_axis',(1.,0.,0.));
#19799=DIRECTION('center_axis',(0.,1.,0.));
#19800=DIRECTION('ref_axis',(1.,0.,0.));
#19801=DIRECTION('center_axis',(0.,1.,0.));
#19802=DIRECTION('ref_axis',(1.,0.,0.));
#19803=DIRECTION('',(0.,-1.,0.));
#19804=DIRECTION('center_axis',(0.,1.,0.));
#19805=DIRECTION('ref_axis',(1.,0.,0.));
#19806=DIRECTION('center_axis',(0.,1.,0.));
#19807=DIRECTION('ref_axis',(1.,0.,0.));
#19808=DIRECTION('',(0.,-1.,0.));
#19809=DIRECTION('center_axis',(0.,1.,0.));
#19810=DIRECTION('ref_axis',(1.,0.,0.));
#19811=DIRECTION('center_axis',(0.,1.,0.));
#19812=DIRECTION('ref_axis',(1.,0.,0.));
#23818=CARTESIAN_POINT('',(0.,0.,0.));
#23819=CARTESIAN_POINT('Origin',(18.056769185842,-4.2,9.30814754519511));
#23820=CARTESIAN_POINT('',(17.706769185842,-4.2,9.30814754519511));
#23821=CARTESIAN_POINT('Origin',(18.056769185842,-4.2,9.30814754519511));
#23822=CARTESIAN_POINT('',(17.856769185842,-4.2,9.30814754519511));
#23823=CARTESIAN_POINT('Origin',(18.056769185842,-4.2,9.30814754519511));
#23824=CARTESIAN_POINT('Origin',(18.056769185842,-4.2,9.30814754519511));
#23825=CARTESIAN_POINT('',(17.706769185842,-4.1,9.30814754519511));
#23826=CARTESIAN_POINT('Origin',(18.056769185842,-4.1,9.30814754519511));
#23827=CARTESIAN_POINT('',(17.706769185842,-4.2,9.30814754519511));
#23828=CARTESIAN_POINT('Origin',(18.056769185842,-4.1,9.30814754519511));
#23829=CARTESIAN_POINT('Origin',(18.056769185842,-4.9,9.30814754519511));
#23830=CARTESIAN_POINT('',(17.856769185842,-4.9,9.30814754519511));
#23831=CARTESIAN_POINT('',(17.856769185842,-4.9,9.30814754519511));
#23832=CARTESIAN_POINT('Origin',(18.056769185842,-4.9,9.30814754519511));
#23833=CARTESIAN_POINT('Origin',(18.056769185842,-4.9,9.30814754519511));
#24950=UNCERTAINTY_MEASURE_WITH_UNIT(LENGTH_MEASURE(0.001),#25101,
'DISTANCE_ACCURACY_VALUE',
'Maximum model space distance between geometric entities at asserted c
onnectivities');
#24979=UNCERTAINTY_MEASURE_WITH_UNIT(LENGTH_MEASURE(0.001),#25101,
'DISTANCE_ACCURACY_VALUE',
'Maximum model space distance between geometric entities at asserted c
onnectivities');
#25071=(
GEOMETRIC_REPRESENTATION_CONTEXT(3)
GLOBAL_UNCERTAINTY_ASSIGNED_CONTEXT((#24950))
GLOBAL_UNIT_ASSIGNED_CONTEXT((#25101,#25103,#25104))
REPRESENTATION_CONTEXT('','3D')
);
#25100=(
GEOMETRIC_REPRESENTATION_CONTEXT(3)
GLOBAL_UNCERTAINTY_ASSIGNED_CONTEXT((#24979))
GLOBAL_UNIT_ASSIGNED_CONTEXT((#25101,#25103,#25104))
REPRESENTATION_CONTEXT('','3D')
);
#25101=(
LENGTH_UNIT()
NAMED_UNIT(*)
SI_UNIT(.CENTI.,.METRE.)
);
#25103=(
NAMED_UNIT(*)
PLANE_ANGLE_UNIT()
SI_UNIT($,.RADIAN.)
);
#25104=(
NAMED_UNIT(*)
SI_UNIT($,.STERADIAN.)
SOLID_ANGLE_UNIT()
);
#25196=SHAPE_DEFINITION_REPRESENTATION(#25390,#25601);
#25390=PRODUCT_DEFINITION_SHAPE('',$,#25722);
#25601=SHAPE_REPRESENTATION('',(#15922),#25071);
#25630=PRODUCT_DEFINITION_CONTEXT('part definition',#25992,'design');
#25722=PRODUCT_DEFINITION('M4 low-profile retaining screw (5)',
'M4 low-profile retaining screw (5)',#25842,#25630);
#25842=PRODUCT_DEFINITION_FORMATION('',$,#26085);
#25992=APPLICATION_CONTEXT(
'Core Data for Automotive Mechanical Design Process');
#25993=PRODUCT_CONTEXT('part definition',#25992,'mechanical');
#26085=PRODUCT('M4 low-profile retaining screw (5)',
'M4 low-profile retaining screw (5)','M4 low-profile retaining screw (5)',(#25993));
#26192=COLOUR_RGB('Black',0.12,0.14,0.17);
#26193=FILL_AREA_STYLE_COLOUR('',#26192);
#26194=FILL_AREA_STYLE('',(#26193));
#26195=SURFACE_STYLE_FILL_AREA(#26194);
#26196=SURFACE_SIDE_STYLE('',(#26195));
#26197=SURFACE_STYLE_USAGE(.BOTH.,#26196);
#26198=PRESENTATION_STYLE_ASSIGNMENT((#26197));
ENDSEC;
END-ISO-10303-21;
